ISO-10303-21;
HEADER;
FILE_DESCRIPTION (('STEP AP214'),
    '1' );
FILE_NAME ('Part 135_Varsay\X2\0131\X0\lan.step',
    '2026-10-08T11:03:28',
    ( '' ),
    ( '' ),
    'SwSTEP 2.0',
    'SolidWorks 2024',
    '' );
FILE_SCHEMA (( 'AUTOMOTIVE_DESIGN' ));
ENDSEC;

DATA;
#96=ORIENTED_EDGE ( 'NONE', *, *, #3980, .T. ) ;
#129=DIRECTION ( 'NONE',  ( 0.000000000000000000, 0.000000000000000000, 1.000000000000000000 ) ) ;
#134=PLANE ( 'NONE',  #2161 ) ;
#210=CARTESIAN_POINT ( 'NONE',  ( 2.316727177394500794E-17, 0.000000000000000000, 1.587499999999999467 ) ) ;
#226=PRESENTATION_STYLE_ASSIGNMENT (( #1341 ) ) ;
#273=DIRECTION ( 'NONE',  ( 0.000000000000000000, 0.000000000000000000, 1.000000000000000000 ) ) ;
#354=VECTOR ( 'NONE', #814, 1000.000000000000000 ) ;
#421=VERTEX_POINT ( 'NONE', #798 ) ;
#483=CYLINDRICAL_SURFACE ( 'NONE', #829, 3.573749999999998650 ) ;
#510=CIRCLE ( 'NONE', #568, 3.573749999999998650 ) ;
#529=ORIENTED_EDGE ( 'NONE', *, *, #4352, .T. ) ;
#568=AXIS2_PLACEMENT_3D ( 'NONE', #4180, #273, #2358 ) ;
#574=( LENGTH_UNIT ( ) NAMED_UNIT ( * ) SI_UNIT ( .MILLI., .METRE. ) );
#605=CARTESIAN_POINT ( 'NONE',  ( 2.316727177394500794E-17, 0.000000000000000000, 1.587499999999999467 ) ) ;
#611=PRODUCT ( 'Part 135_Varsay\X2\0131\X0\lan', 'Part 135_Varsay\X2\0131\X0\lan', '', ( #3231 ) ) ;
#615=ORIENTED_EDGE ( 'NONE', *, *, #4312, .F. ) ;
#624=( NAMED_UNIT ( * ) PLANE_ANGLE_UNIT ( ) SI_UNIT ( $, .RADIAN. ) );
#650=DIRECTION ( 'NONE',  ( 0.000000000000000000, 0.000000000000000000, 1.000000000000000000 ) ) ;
#798=CARTESIAN_POINT ( 'NONE',  ( 3.573749999999998650, 4.376581498452851814E-16, 11.11249999999999893 ) ) ;
#814=DIRECTION ( 'NONE',  ( -0.000000000000000000, -0.000000000000000000, -1.000000000000000000 ) ) ;
#815=EDGE_LOOP ( 'NONE', ( #4486, #2215 ) ) ;
#829=AXIS2_PLACEMENT_3D ( 'NONE', #3408, #3755, #2694 ) ;
#886=FACE_OUTER_BOUND ( 'NONE', #2438, .T. ) ;
#906=UNCERTAINTY_MEASURE_WITH_UNIT (LENGTH_MEASURE( 1.000000000000000082E-05 ), #574, 'distance_accuracy_value', 'NONE');
#1059=ORIENTED_EDGE ( 'NONE', *, *, #2895, .T. ) ;
#1119=ORIENTED_EDGE ( 'NONE', *, *, #4312, .T. ) ;
#1126=AXIS2_PLACEMENT_3D ( 'NONE', #4195, #3775, #2419 ) ;
#1141=AXIS2_PLACEMENT_3D ( 'NONE', #605, #650, #3847 ) ;
#1232=DIRECTION ( 'NONE',  ( 1.000000000000000000, 0.000000000000000000, -0.000000000000000000 ) ) ;
#1260=CLOSED_SHELL ( 'NONE', ( #1998, #3537, #1318, #4254 ) ) ;
#1286=DIRECTION ( 'NONE',  ( -0.000000000000000000, -0.000000000000000000, -1.000000000000000000 ) ) ;
#1318=ADVANCED_FACE ( 'NONE', ( #2788 ), #1346, .T. ) ;
#1337=FACE_OUTER_BOUND ( 'NONE', #4167, .T. ) ;
#1341=SURFACE_STYLE_USAGE ( .BOTH. , #3823 ) ;
#1346=PLANE ( 'NONE',  #3384 ) ;
#1375=EDGE_CURVE ( 'NONE', #3489, #3350, #3759, .T. ) ;
#1403=ORIENTED_EDGE ( 'NONE', *, *, #3980, .F. ) ;
#1571=AXIS2_PLACEMENT_3D ( 'NONE', #1705, #3467, #2054 ) ;
#1632=ADVANCED_BREP_SHAPE_REPRESENTATION ( '', ( #1876, #4483 ), #3573 ) ;
#1674=CYLINDRICAL_SURFACE ( 'NONE', #1126, 3.573749999999998650 ) ;
#1679=CARTESIAN_POINT ( 'NONE',  ( -3.573749999999998650, 0.000000000000000000, 1.587499999999999467 ) ) ;
#1683=CARTESIAN_POINT ( 'NONE',  ( 2.316727177394500794E-17, 0.000000000000000000, 11.11249999999999893 ) ) ;
#1705=CARTESIAN_POINT ( 'NONE',  ( 2.316727177394500794E-17, 0.000000000000000000, 11.11249999999999893 ) ) ;
#1707=PRODUCT_DEFINITION_FORMATION_WITH_SPECIFIED_SOURCE ( 'ANY', '', #611, .NOT_KNOWN. ) ;
#1808=SHAPE_DEFINITION_REPRESENTATION ( #4559, #2171 ) ;
#1822=VERTEX_POINT ( 'NONE', #3799 ) ;
#1865=VECTOR ( 'NONE', #1286, 1000.000000000000000 ) ;
#1876=MANIFOLD_SOLID_BREP ( 'Ölçek1', #1260 ) ;
#1998=ADVANCED_FACE ( 'NONE', ( #886 ), #483, .T. ) ;
#2054=DIRECTION ( 'NONE',  ( 1.000000000000000000, 0.000000000000000000, 0.000000000000000000 ) ) ;
#2161=AXIS2_PLACEMENT_3D ( 'NONE', #210, #3000, #1232 ) ;
#2171=SHAPE_REPRESENTATION ( 'Part 135_Varsay\X2\0131\X0\lan', ( #4483 ), #3573 ) ;
#2215=ORIENTED_EDGE ( 'NONE', *, *, #1375, .F. ) ;
#2257=COLOUR_RGB ( '', 0.72549020, 0.75294118, 0.79215686) ;
#2302=CIRCLE ( 'NONE', #1571, 3.573749999999998650 ) ;
#2358=DIRECTION ( 'NONE',  ( 1.000000000000000000, 0.000000000000000000, 0.000000000000000000 ) ) ;
#2419=DIRECTION ( 'NONE',  ( -1.000000000000000000, 0.000000000000000000, 0.000000000000000000 ) ) ;
#2438=EDGE_LOOP ( 'NONE', ( #615, #1059, #4266, #2802 ) ) ;
#2551=LINE ( 'NONE', #3337, #354 ) ;
#2552=EDGE_CURVE ( 'NONE', #1822, #3350, #2551, .T. ) ;
#2694=DIRECTION ( 'NONE',  ( -1.000000000000000000, 0.000000000000000000, 0.000000000000000000 ) ) ;
#2769=LINE ( 'NONE', #3790, #1865 ) ;
#2783=( NAMED_UNIT ( * ) SI_UNIT ( $, .STERADIAN. ) SOLID_ANGLE_UNIT ( ) );
#2788=FACE_OUTER_BOUND ( 'NONE', #4647, .T. ) ;
#2802=ORIENTED_EDGE ( 'NONE', *, *, #2552, .F. ) ;
#2818=CIRCLE ( 'NONE', #4633, 3.573749999999998650 ) ;
#2895=EDGE_CURVE ( 'NONE', #421, #3489, #2769, .T. ) ;
#3000=DIRECTION ( 'NONE',  ( 0.000000000000000000, 0.000000000000000000, 1.000000000000000000 ) ) ;
#3064=UNCERTAINTY_MEASURE_WITH_UNIT (LENGTH_MEASURE( 1.000000000000000082E-05 ), #3191, 'distance_accuracy_value', 'NONE');
#3069=( NAMED_UNIT ( * ) PLANE_ANGLE_UNIT ( ) SI_UNIT ( $, .RADIAN. ) );
#3138=( NAMED_UNIT ( * ) SI_UNIT ( $, .STERADIAN. ) SOLID_ANGLE_UNIT ( ) );
#3145=DIRECTION ( 'NONE',  ( 1.000000000000000000, 0.000000000000000000, 0.000000000000000000 ) ) ;
#3191=( LENGTH_UNIT ( ) NAMED_UNIT ( * ) SI_UNIT ( .MILLI., .METRE. ) );
#3231=PRODUCT_CONTEXT ( 'NONE', #3358, 'mechanical' ) ;
#3241=MECHANICAL_DESIGN_GEOMETRIC_PRESENTATION_REPRESENTATION('',(#4292),#3315);
#3297=PRODUCT_DEFINITION ( 'UNKNOWN', '', #1707, #4474 ) ;
#3315=( GEOMETRIC_REPRESENTATION_CONTEXT ( 3 ) GLOBAL_UNCERTAINTY_ASSIGNED_CONTEXT ( ( #3064 ) ) GLOBAL_UNIT_ASSIGNED_CONTEXT ( ( #3191, #624, #2783 ) ) REPRESENTATION_CONTEXT ( 'NONE', 'WORKASPACE' ) );
#3337=CARTESIAN_POINT ( 'NONE',  ( -3.573749999999998650, 0.000000000000000000, 11.11249999999999893 ) ) ;
#3350=VERTEX_POINT ( 'NONE', #1679 ) ;
#3358=APPLICATION_CONTEXT ( 'automotive_design' ) ;
#3384=AXIS2_PLACEMENT_3D ( 'NONE', #1683, #3486, #3869 ) ;
#3404=CARTESIAN_POINT ( 'NONE',  ( 3.573749999999998650, 4.376581498452851814E-16, 1.587499999999999467 ) ) ;
#3408=CARTESIAN_POINT ( 'NONE',  ( 2.316727177394500794E-17, 0.000000000000000000, 11.11249999999999893 ) ) ;
#3450=ORIENTED_EDGE ( 'NONE', *, *, #2895, .F. ) ;
#3454=APPLICATION_CONTEXT ( 'automotive_design' ) ;
#3467=DIRECTION ( 'NONE',  ( 0.000000000000000000, 0.000000000000000000, 1.000000000000000000 ) ) ;
#3478=SHAPE_REPRESENTATION_RELATIONSHIP ( 'NONE' , 'NONE' ,  #2171, #1632 ) ;
#3486=DIRECTION ( 'NONE',  ( 0.000000000000000000, 0.000000000000000000, 1.000000000000000000 ) ) ;
#3489=VERTEX_POINT ( 'NONE', #3404 ) ;
#3521=FILL_AREA_STYLE_COLOUR ( '', #2257 ) ;
#3537=ADVANCED_FACE ( 'NONE', ( #1337 ), #1674, .T. ) ;
#3573=( GEOMETRIC_REPRESENTATION_CONTEXT ( 3 ) GLOBAL_UNCERTAINTY_ASSIGNED_CONTEXT ( ( #906 ) ) GLOBAL_UNIT_ASSIGNED_CONTEXT ( ( #574, #3069, #3138 ) ) REPRESENTATION_CONTEXT ( 'NONE', 'WORKASPACE' ) );
#3704=DIRECTION ( 'NONE',  ( 1.000000000000000000, 0.000000000000000000, 0.000000000000000000 ) ) ;
#3752=CARTESIAN_POINT ( 'NONE',  ( 0.000000000000000000, 0.000000000000000000, 0.000000000000000000 ) ) ;
#3755=DIRECTION ( 'NONE',  ( -0.000000000000000000, -0.000000000000000000, -1.000000000000000000 ) ) ;
#3759=CIRCLE ( 'NONE', #1141, 3.573749999999998650 ) ;
#3775=DIRECTION ( 'NONE',  ( -0.000000000000000000, -0.000000000000000000, -1.000000000000000000 ) ) ;
#3790=CARTESIAN_POINT ( 'NONE',  ( 3.573749999999998650, 4.376581498452851814E-16, 11.11249999999999893 ) ) ;
#3799=CARTESIAN_POINT ( 'NONE',  ( -3.573749999999998650, 0.000000000000000000, 11.11249999999999893 ) ) ;
#3803=ORIENTED_EDGE ( 'NONE', *, *, #2552, .T. ) ;
#3823=SURFACE_SIDE_STYLE ('',( #4556 ) ) ;
#3826=CARTESIAN_POINT ( 'NONE',  ( 2.316727177394500794E-17, 0.000000000000000000, 1.587499999999999467 ) ) ;
#3847=DIRECTION ( 'NONE',  ( 1.000000000000000000, 0.000000000000000000, 0.000000000000000000 ) ) ;
#3869=DIRECTION ( 'NONE',  ( 1.000000000000000000, 0.000000000000000000, -0.000000000000000000 ) ) ;
#3891=FILL_AREA_STYLE ('',( #3521 ) ) ;
#3895=DIRECTION ( 'NONE',  ( 0.000000000000000000, 0.000000000000000000, 1.000000000000000000 ) ) ;
#3980=EDGE_CURVE ( 'NONE', #1822, #421, #2302, .T. ) ;
#4167=EDGE_LOOP ( 'NONE', ( #3450, #1403, #3803, #529 ) ) ;
#4180=CARTESIAN_POINT ( 'NONE',  ( 2.316727177394500794E-17, 0.000000000000000000, 11.11249999999999893 ) ) ;
#4195=CARTESIAN_POINT ( 'NONE',  ( 2.316727177394500794E-17, 0.000000000000000000, 11.11249999999999893 ) ) ;
#4254=ADVANCED_FACE ( 'NONE', ( #4468 ), #134, .F. ) ;
#4266=ORIENTED_EDGE ( 'NONE', *, *, #1375, .T. ) ;
#4292=STYLED_ITEM ( 'NONE', ( #226 ), #1876 ) ;
#4312=EDGE_CURVE ( 'NONE', #421, #1822, #510, .T. ) ;
#4352=EDGE_CURVE ( 'NONE', #3350, #3489, #2818, .T. ) ;
#4468=FACE_OUTER_BOUND ( 'NONE', #815, .T. ) ;
#4474=PRODUCT_DEFINITION_CONTEXT ( 'detailed design', #3454, 'design' ) ;
#4483=AXIS2_PLACEMENT_3D ( 'NONE', #3752, #129, #3704 ) ;
#4486=ORIENTED_EDGE ( 'NONE', *, *, #4352, .F. ) ;
#4556=SURFACE_STYLE_FILL_AREA ( #3891 ) ;
#4559=PRODUCT_DEFINITION_SHAPE ( 'NONE', 'NONE',  #3297 ) ;
#4633=AXIS2_PLACEMENT_3D ( 'NONE', #3826, #3895, #3145 ) ;
#4647=EDGE_LOOP ( 'NONE', ( #96, #1119 ) ) ;
ENDSEC;
END-ISO-10303-21;
